ISO-10303-21;
HEADER;
/* Generated by software containing ST-Developer
 * from STEP Tools, Inc. (www.steptools.com) 
 */

FILE_DESCRIPTION(
/* description */ ('Cam-and-follower valve demonstrator'),
/* implementation_level */ '2;1');

FILE_NAME(
/* name */ 'Cap Screw - M5x20.step',
/* time_stamp */ '2026-10-28T03:25:17-07:00',
/* author */ (''),
/* organization */ (''),
/* preprocessor_version */ 'ST-DEVELOPER v20.2',
/* originating_system */ 'Autodesk Translation Framework v15.17.0.0',
/* authorisation */ '');

FILE_SCHEMA (('AUTOMOTIVE_DESIGN { 1 0 10303 214 3 1 1 }'));
ENDSEC;

DATA;
#10=MECHANICAL_DESIGN_GEOMETRIC_PRESENTATION_REPRESENTATION('',(#436),#12896);
#11=ORIENTED_CLOSED_SHELL('',*,#6204,.F.);
#14=BREP_WITH_VOIDS('Body1',#6203,(#11));
#311=CONICAL_SURFACE('',#7045,0.4,0.785398163397448);
#312=CONICAL_SURFACE('',#7049,0.41,0.785398163397448);
#313=CONICAL_SURFACE('',#7053,0.26,0.463647609000806);
#314=CONICAL_SURFACE('',#7057,0.225,0.785398163397448);
#357=SHAPE_REPRESENTATION_RELATIONSHIP('SRR','None',#13074,#393);
#393=ADVANCED_BREP_SHAPE_REPRESENTATION('',(#14),#12874);
#436=STYLED_ITEM('',(#13337),#14);
#613=FACE_BOUND('',#1781,.T.);
#860=CIRCLE('',#7044,0.375);
#861=CIRCLE('',#7046,0.425);
#862=CIRCLE('',#7048,0.425);
#863=CIRCLE('',#7050,0.395);
#864=CIRCLE('',#7052,0.27);
#865=CIRCLE('',#7054,0.24505);
#866=CIRCLE('',#7056,0.24505);
#867=CIRCLE('',#7058,0.2);
#1050=CYLINDRICAL_SURFACE('',#7047,0.425);
#1051=CYLINDRICAL_SURFACE('',#7055,0.24505);
#1290=FACE_OUTER_BOUND('',#1776,.T.);
#1291=FACE_OUTER_BOUND('',#1777,.T.);
#1292=FACE_OUTER_BOUND('',#1778,.T.);
#1293=FACE_OUTER_BOUND('',#1779,.T.);
#1294=FACE_OUTER_BOUND('',#1780,.T.);
#1295=FACE_OUTER_BOUND('',#1782,.T.);
#1296=FACE_OUTER_BOUND('',#1783,.T.);
#1297=FACE_OUTER_BOUND('',#1784,.T.);
#1298=FACE_OUTER_BOUND('',#1785,.T.);
#1299=FACE_OUTER_BOUND('',#1786,.T.);
#1300=FACE_OUTER_BOUND('',#1787,.T.);
#1301=FACE_OUTER_BOUND('',#1788,.T.);
#1302=FACE_OUTER_BOUND('',#1789,.T.);
#1303=FACE_OUTER_BOUND('',#1790,.T.);
#1304=FACE_OUTER_BOUND('',#1791,.T.);
#1305=FACE_OUTER_BOUND('',#1792,.T.);
#1306=FACE_OUTER_BOUND('',#1793,.T.);
#1776=EDGE_LOOP('',(#4953));
#1777=EDGE_LOOP('',(#4954,#4955,#4956,#4957));
#1778=EDGE_LOOP('',(#4958,#4959,#4960,#4961));
#1779=EDGE_LOOP('',(#4962,#4963,#4964,#4965));
#1780=EDGE_LOOP('',(#4966));
#1781=EDGE_LOOP('',(#4967));
#1782=EDGE_LOOP('',(#4968,#4969,#4970,#4971));
#1783=EDGE_LOOP('',(#4972,#4973,#4974,#4975));
#1784=EDGE_LOOP('',(#4976,#4977,#4978,#4979));
#1785=EDGE_LOOP('',(#4980));
#1786=EDGE_LOOP('',(#4981,#4982,#4983,#4984));
#1787=EDGE_LOOP('',(#4985,#4986,#4987,#4988));
#1788=EDGE_LOOP('',(#4989,#4990,#4991,#4992));
#1789=EDGE_LOOP('',(#4993,#4994,#4995,#4996));
#1790=EDGE_LOOP('',(#4997,#4998,#4999,#5000));
#1791=EDGE_LOOP('',(#5001,#5002,#5003,#5004));
#1792=EDGE_LOOP('',(#5005,#5006,#5007,#5008,#5009,#5010));
#1793=EDGE_LOOP('',(#5011,#5012,#5013,#5014,#5015,#5016));
#2208=LINE('',#12026,#2630);
#2209=LINE('',#12030,#2631);
#2210=LINE('',#12034,#2632);
#2211=LINE('',#12041,#2633);
#2212=LINE('',#12045,#2634);
#2213=LINE('',#12049,#2635);
#2214=LINE('',#12054,#2636);
#2215=LINE('',#12056,#2637);
#2216=LINE('',#12058,#2638);
#2217=LINE('',#12059,#2639);
#2218=LINE('',#12062,#2640);
#2219=LINE('',#12064,#2641);
#2220=LINE('',#12065,#2642);
#2221=LINE('',#12068,#2643);
#2222=LINE('',#12070,#2644);
#2223=LINE('',#12071,#2645);
#2224=LINE('',#12074,#2646);
#2225=LINE('',#12076,#2647);
#2226=LINE('',#12077,#2648);
#2227=LINE('',#12080,#2649);
#2228=LINE('',#12082,#2650);
#2229=LINE('',#12083,#2651);
#2230=LINE('',#12085,#2652);
#2231=LINE('',#12086,#2653);
#2630=VECTOR('',#8477,0.4);
#2631=VECTOR('',#8482,0.425);
#2632=VECTOR('',#8487,0.41);
#2633=VECTOR('',#8496,0.26);
#2634=VECTOR('',#8501,0.25);
#2635=VECTOR('',#8506,0.225);
#2636=VECTOR('',#8511,1.);
#2637=VECTOR('',#8512,1.);
#2638=VECTOR('',#8513,1.);
#2639=VECTOR('',#8514,1.);
#2640=VECTOR('',#8517,1.);
#2641=VECTOR('',#8518,1.);
#2642=VECTOR('',#8519,1.);
#2643=VECTOR('',#8522,1.);
#2644=VECTOR('',#8523,1.);
#2645=VECTOR('',#8524,1.);
#2646=VECTOR('',#8527,1.);
#2647=VECTOR('',#8528,1.);
#2648=VECTOR('',#8529,1.);
#2649=VECTOR('',#8532,1.);
#2650=VECTOR('',#8533,1.);
#2651=VECTOR('',#8534,1.);
#2652=VECTOR('',#8537,1.);
#2653=VECTOR('',#8538,1.);
#3133=VERTEX_POINT('',#12021);
#3134=VERTEX_POINT('',#12024);
#3135=VERTEX_POINT('',#12028);
#3136=VERTEX_POINT('',#12032);
#3137=VERTEX_POINT('',#12036);
#3138=VERTEX_POINT('',#12039);
#3139=VERTEX_POINT('',#12043);
#3140=VERTEX_POINT('',#12047);
#3141=VERTEX_POINT('',#12052);
#3142=VERTEX_POINT('',#12053);
#3143=VERTEX_POINT('',#12055);
#3144=VERTEX_POINT('',#12057);
#3145=VERTEX_POINT('',#12061);
#3146=VERTEX_POINT('',#12063);
#3147=VERTEX_POINT('',#12067);
#3148=VERTEX_POINT('',#12069);
#3149=VERTEX_POINT('',#12073);
#3150=VERTEX_POINT('',#12075);
#3151=VERTEX_POINT('',#12079);
#3152=VERTEX_POINT('',#12081);
#3773=EDGE_CURVE('',#3133,#3133,#860,.T.);
#3774=EDGE_CURVE('',#3134,#3134,#861,.T.);
#3775=EDGE_CURVE('',#3134,#3133,#2208,.T.);
#3776=EDGE_CURVE('',#3135,#3135,#862,.T.);
#3777=EDGE_CURVE('',#3135,#3134,#2209,.T.);
#3778=EDGE_CURVE('',#3136,#3136,#863,.T.);
#3779=EDGE_CURVE('',#3136,#3135,#2210,.T.);
#3780=EDGE_CURVE('',#3137,#3137,#864,.T.);
#3781=EDGE_CURVE('',#3138,#3138,#865,.F.);
#3782=EDGE_CURVE('',#3138,#3137,#2211,.T.);
#3783=EDGE_CURVE('',#3139,#3139,#866,.F.);
#3784=EDGE_CURVE('',#3139,#3138,#2212,.T.);
#3785=EDGE_CURVE('',#3140,#3140,#867,.T.);
#3786=EDGE_CURVE('',#3140,#3139,#2213,.T.);
#3787=EDGE_CURVE('',#3141,#3142,#2214,.T.);
#3788=EDGE_CURVE('',#3142,#3143,#2215,.T.);
#3789=EDGE_CURVE('',#3143,#3144,#2216,.T.);
#3790=EDGE_CURVE('',#3141,#3144,#2217,.T.);
#3791=EDGE_CURVE('',#3142,#3145,#2218,.T.);
#3792=EDGE_CURVE('',#3145,#3146,#2219,.T.);
#3793=EDGE_CURVE('',#3146,#3143,#2220,.T.);
#3794=EDGE_CURVE('',#3145,#3147,#2221,.T.);
#3795=EDGE_CURVE('',#3147,#3148,#2222,.T.);
#3796=EDGE_CURVE('',#3148,#3146,#2223,.T.);
#3797=EDGE_CURVE('',#3147,#3149,#2224,.T.);
#3798=EDGE_CURVE('',#3149,#3150,#2225,.T.);
#3799=EDGE_CURVE('',#3150,#3148,#2226,.T.);
#3800=EDGE_CURVE('',#3149,#3151,#2227,.T.);
#3801=EDGE_CURVE('',#3151,#3152,#2228,.T.);
#3802=EDGE_CURVE('',#3152,#3150,#2229,.T.);
#3803=EDGE_CURVE('',#3151,#3141,#2230,.T.);
#3804=EDGE_CURVE('',#3144,#3152,#2231,.T.);
#4953=ORIENTED_EDGE('',*,*,#3773,.F.);
#4954=ORIENTED_EDGE('',*,*,#3774,.F.);
#4955=ORIENTED_EDGE('',*,*,#3775,.T.);
#4956=ORIENTED_EDGE('',*,*,#3773,.T.);
#4957=ORIENTED_EDGE('',*,*,#3775,.F.);
#4958=ORIENTED_EDGE('',*,*,#3776,.F.);
#4959=ORIENTED_EDGE('',*,*,#3777,.T.);
#4960=ORIENTED_EDGE('',*,*,#3774,.T.);
#4961=ORIENTED_EDGE('',*,*,#3777,.F.);
#4962=ORIENTED_EDGE('',*,*,#3778,.F.);
#4963=ORIENTED_EDGE('',*,*,#3779,.T.);
#4964=ORIENTED_EDGE('',*,*,#3776,.T.);
#4965=ORIENTED_EDGE('',*,*,#3779,.F.);
#4966=ORIENTED_EDGE('',*,*,#3778,.T.);
#4967=ORIENTED_EDGE('',*,*,#3780,.F.);
#4968=ORIENTED_EDGE('',*,*,#3781,.F.);
#4969=ORIENTED_EDGE('',*,*,#3782,.T.);
#4970=ORIENTED_EDGE('',*,*,#3780,.T.);
#4971=ORIENTED_EDGE('',*,*,#3782,.F.);
#4972=ORIENTED_EDGE('',*,*,#3783,.F.);
#4973=ORIENTED_EDGE('',*,*,#3784,.T.);
#4974=ORIENTED_EDGE('',*,*,#3781,.T.);
#4975=ORIENTED_EDGE('',*,*,#3784,.F.);
#4976=ORIENTED_EDGE('',*,*,#3785,.F.);
#4977=ORIENTED_EDGE('',*,*,#3786,.T.);
#4978=ORIENTED_EDGE('',*,*,#3783,.T.);
#4979=ORIENTED_EDGE('',*,*,#3786,.F.);
#4980=ORIENTED_EDGE('',*,*,#3785,.T.);
#4981=ORIENTED_EDGE('',*,*,#3787,.T.);
#4982=ORIENTED_EDGE('',*,*,#3788,.T.);
#4983=ORIENTED_EDGE('',*,*,#3789,.T.);
#4984=ORIENTED_EDGE('',*,*,#3790,.F.);
#4985=ORIENTED_EDGE('',*,*,#3791,.T.);
#4986=ORIENTED_EDGE('',*,*,#3792,.T.);
#4987=ORIENTED_EDGE('',*,*,#3793,.T.);
#4988=ORIENTED_EDGE('',*,*,#3788,.F.);
#4989=ORIENTED_EDGE('',*,*,#3794,.T.);
#4990=ORIENTED_EDGE('',*,*,#3795,.T.);
#4991=ORIENTED_EDGE('',*,*,#3796,.T.);
#4992=ORIENTED_EDGE('',*,*,#3792,.F.);
#4993=ORIENTED_EDGE('',*,*,#3797,.T.);
#4994=ORIENTED_EDGE('',*,*,#3798,.T.);
#4995=ORIENTED_EDGE('',*,*,#3799,.T.);
#4996=ORIENTED_EDGE('',*,*,#3795,.F.);
#4997=ORIENTED_EDGE('',*,*,#3800,.T.);
#4998=ORIENTED_EDGE('',*,*,#3801,.T.);
#4999=ORIENTED_EDGE('',*,*,#3802,.T.);
#5000=ORIENTED_EDGE('',*,*,#3798,.F.);
#5001=ORIENTED_EDGE('',*,*,#3803,.T.);
#5002=ORIENTED_EDGE('',*,*,#3790,.T.);
#5003=ORIENTED_EDGE('',*,*,#3804,.T.);
#5004=ORIENTED_EDGE('',*,*,#3801,.F.);
#5005=ORIENTED_EDGE('',*,*,#3803,.F.);
#5006=ORIENTED_EDGE('',*,*,#3800,.F.);
#5007=ORIENTED_EDGE('',*,*,#3797,.F.);
#5008=ORIENTED_EDGE('',*,*,#3794,.F.);
#5009=ORIENTED_EDGE('',*,*,#3791,.F.);
#5010=ORIENTED_EDGE('',*,*,#3787,.F.);
#5011=ORIENTED_EDGE('',*,*,#3804,.F.);
#5012=ORIENTED_EDGE('',*,*,#3789,.F.);
#5013=ORIENTED_EDGE('',*,*,#3793,.F.);
#5014=ORIENTED_EDGE('',*,*,#3796,.F.);
#5015=ORIENTED_EDGE('',*,*,#3799,.F.);
#5016=ORIENTED_EDGE('',*,*,#3802,.F.);
#5694=PLANE('',#7043);
#5695=PLANE('',#7051);
#5696=PLANE('',#7059);
#5697=PLANE('',#7060);
#5698=PLANE('',#7061);
#5699=PLANE('',#7062);
#5700=PLANE('',#7063);
#5701=PLANE('',#7064);
#5702=PLANE('',#7065);
#5703=PLANE('',#7066);
#5704=PLANE('',#7067);
#6006=ADVANCED_FACE('',(#1290),#5694,.T.);
#6007=ADVANCED_FACE('',(#1291),#311,.T.);
#6008=ADVANCED_FACE('',(#1292),#1050,.T.);
#6009=ADVANCED_FACE('',(#1293),#312,.T.);
#6010=ADVANCED_FACE('',(#1294,#613),#5695,.T.);
#6011=ADVANCED_FACE('',(#1295),#313,.T.);
#6012=ADVANCED_FACE('',(#1296),#1051,.T.);
#6013=ADVANCED_FACE('',(#1297),#314,.T.);
#6014=ADVANCED_FACE('',(#1298),#5696,.T.);
#6015=ADVANCED_FACE('',(#1299),#5697,.F.);
#6016=ADVANCED_FACE('',(#1300),#5698,.F.);
#6017=ADVANCED_FACE('',(#1301),#5699,.F.);
#6018=ADVANCED_FACE('',(#1302),#5700,.F.);
#6019=ADVANCED_FACE('',(#1303),#5701,.F.);
#6020=ADVANCED_FACE('',(#1304),#5702,.F.);
#6021=ADVANCED_FACE('',(#1305),#5703,.F.);
#6022=ADVANCED_FACE('',(#1306),#5704,.F.);
#6203=CLOSED_SHELL('',(#6006,#6007,#6008,#6009,#6010,#6011,#6012,#6013,
#6014));
#6204=CLOSED_SHELL('',(#6015,#6016,#6017,#6018,#6019,#6020,#6021,#6022));
#7042=AXIS2_PLACEMENT_3D('',#12019,#8467,#8468);
#7043=AXIS2_PLACEMENT_3D('',#12020,#8469,#8470);
#7044=AXIS2_PLACEMENT_3D('',#12022,#8471,#8472);
#7045=AXIS2_PLACEMENT_3D('',#12023,#8473,#8474);
#7046=AXIS2_PLACEMENT_3D('',#12025,#8475,#8476);
#7047=AXIS2_PLACEMENT_3D('',#12027,#8478,#8479);
#7048=AXIS2_PLACEMENT_3D('',#12029,#8480,#8481);
#7049=AXIS2_PLACEMENT_3D('',#12031,#8483,#8484);
#7050=AXIS2_PLACEMENT_3D('',#12033,#8485,#8486);
#7051=AXIS2_PLACEMENT_3D('',#12035,#8488,#8489);
#7052=AXIS2_PLACEMENT_3D('',#12037,#8490,#8491);
#7053=AXIS2_PLACEMENT_3D('',#12038,#8492,#8493);
#7054=AXIS2_PLACEMENT_3D('',#12040,#8494,#8495);
#7055=AXIS2_PLACEMENT_3D('',#12042,#8497,#8498);
#7056=AXIS2_PLACEMENT_3D('',#12044,#8499,#8500);
#7057=AXIS2_PLACEMENT_3D('',#12046,#8502,#8503);
#7058=AXIS2_PLACEMENT_3D('',#12048,#8504,#8505);
#7059=AXIS2_PLACEMENT_3D('',#12050,#8507,#8508);
#7060=AXIS2_PLACEMENT_3D('',#12051,#8509,#8510);
#7061=AXIS2_PLACEMENT_3D('',#12060,#8515,#8516);
#7062=AXIS2_PLACEMENT_3D('',#12066,#8520,#8521);
#7063=AXIS2_PLACEMENT_3D('',#12072,#8525,#8526);
#7064=AXIS2_PLACEMENT_3D('',#12078,#8530,#8531);
#7065=AXIS2_PLACEMENT_3D('',#12084,#8535,#8536);
#7066=AXIS2_PLACEMENT_3D('',#12087,#8539,#8540);
#7067=AXIS2_PLACEMENT_3D('',#12088,#8541,#8542);
#8467=DIRECTION('axis',(0.,0.,1.));
#8468=DIRECTION('refdir',(1.,0.,0.));
#8469=DIRECTION('center_axis',(0.,1.,0.));
#8470=DIRECTION('ref_axis',(0.,0.,1.));
#8471=DIRECTION('center_axis',(0.,-1.,0.));
#8472=DIRECTION('ref_axis',(1.,0.,0.));
#8473=DIRECTION('center_axis',(0.,-1.,0.));
#8474=DIRECTION('ref_axis',(1.,0.,0.));
#8475=DIRECTION('center_axis',(0.,-1.,0.));
#8476=DIRECTION('ref_axis',(1.,0.,0.));
#8477=DIRECTION('',(0.707106781186548,0.707106781186547,8.65956056235493E-17));
#8478=DIRECTION('center_axis',(0.,-1.,0.));
#8479=DIRECTION('ref_axis',(1.,0.,0.));
#8480=DIRECTION('center_axis',(0.,-1.,0.));
#8481=DIRECTION('ref_axis',(1.,0.,0.));
#8482=DIRECTION('',(0.,1.,0.));
#8483=DIRECTION('center_axis',(0.,1.,0.));
#8484=DIRECTION('ref_axis',(1.,0.,0.));
#8485=DIRECTION('center_axis',(0.,-1.,0.));
#8486=DIRECTION('ref_axis',(1.,0.,0.));
#8487=DIRECTION('',(-0.707106781186547,0.707106781186548,-8.65956056235493E-17));
#8488=DIRECTION('center_axis',(0.,-1.,0.));
#8489=DIRECTION('ref_axis',(0.,0.,-1.));
#8490=DIRECTION('center_axis',(0.,-1.,0.));
#8491=DIRECTION('ref_axis',(1.,0.,0.));
#8492=DIRECTION('center_axis',(0.,1.,0.));
#8493=DIRECTION('ref_axis',(1.,0.,0.));
#8494=DIRECTION('center_axis',(0.,1.,0.));
#8495=DIRECTION('ref_axis',(1.,0.,0.));
#8496=DIRECTION('',(-0.447213595499958,0.894427190999916,-5.47678698264203E-17));
#8497=DIRECTION('center_axis',(0.,-1.,0.));
#8498=DIRECTION('ref_axis',(1.,0.,0.));
#8499=DIRECTION('center_axis',(0.,1.,0.));
#8500=DIRECTION('ref_axis',(1.,0.,0.));
#8501=DIRECTION('',(0.,1.,0.));
#8502=DIRECTION('center_axis',(0.,1.,0.));
#8503=DIRECTION('ref_axis',(1.,0.,0.));
#8504=DIRECTION('center_axis',(0.,-1.,0.));
#8505=DIRECTION('ref_axis',(1.,0.,0.));
#8506=DIRECTION('',(-0.707106781186547,0.707106781186548,-8.65956056235493E-17));
#8507=DIRECTION('center_axis',(0.,-1.,0.));
#8508=DIRECTION('ref_axis',(0.,0.,-1.));
#8509=DIRECTION('center_axis',(0.866025403784439,0.,-0.5));
#8510=DIRECTION('ref_axis',(0.5,0.,0.866025403784439));
#8511=DIRECTION('',(-0.5,0.,-0.866025403784439));
#8512=DIRECTION('',(0.,-1.,0.));
#8513=DIRECTION('',(0.5,0.,0.866025403784439));
#8514=DIRECTION('',(0.,-1.,0.));
#8515=DIRECTION('center_axis',(1.20185167898973E-16,0.,-1.));
#8516=DIRECTION('ref_axis',(1.,0.,1.20185167898973E-16));
#8517=DIRECTION('',(-1.,0.,-1.20185167898973E-16));
#8518=DIRECTION('',(0.,-1.,0.));
#8519=DIRECTION('',(1.,0.,1.20185167898973E-16));
#8520=DIRECTION('center_axis',(-0.866025403784439,0.,-0.5));
#8521=DIRECTION('ref_axis',(0.5,0.,-0.866025403784439));
#8522=DIRECTION('',(-0.5,0.,0.866025403784439));
#8523=DIRECTION('',(0.,-1.,0.));
#8524=DIRECTION('',(0.5,0.,-0.866025403784439));
#8525=DIRECTION('center_axis',(-0.866025403784439,0.,0.5));
#8526=DIRECTION('ref_axis',(-0.5,0.,-0.866025403784439));
#8527=DIRECTION('',(0.5,0.,0.866025403784439));
#8528=DIRECTION('',(0.,-1.,0.));
#8529=DIRECTION('',(-0.5,0.,-0.866025403784439));
#8530=DIRECTION('center_axis',(-2.40370335797945E-16,0.,1.));
#8531=DIRECTION('ref_axis',(-1.,0.,-2.40370335797945E-16));
#8532=DIRECTION('',(1.,0.,2.40370335797945E-16));
#8533=DIRECTION('',(0.,-1.,0.));
#8534=DIRECTION('',(-1.,0.,-2.40370335797945E-16));
#8535=DIRECTION('center_axis',(0.866025403784439,0.,0.5));
#8536=DIRECTION('ref_axis',(-0.5,0.,0.866025403784439));
#8537=DIRECTION('',(0.5,0.,-0.866025403784439));
#8538=DIRECTION('',(-0.5,0.,0.866025403784439));
#8539=DIRECTION('center_axis',(0.,1.,0.));
#8540=DIRECTION('ref_axis',(1.,0.,0.));
#8541=DIRECTION('center_axis',(0.,-1.,0.));
#8542=DIRECTION('ref_axis',(0.,0.,-1.));
#12019=CARTESIAN_POINT('',(0.,0.,0.));
#12020=CARTESIAN_POINT('Origin',(0.375,0.5,0.));
#12021=CARTESIAN_POINT('',(-0.375,0.5,-4.59242549680257E-17));
#12022=CARTESIAN_POINT('Origin',(0.,0.5,0.));
#12023=CARTESIAN_POINT('Origin',(0.,0.475,0.));
#12024=CARTESIAN_POINT('',(-0.425,0.45,-5.20474889637625E-17));
#12025=CARTESIAN_POINT('Origin',(0.,0.45,0.));
#12026=CARTESIAN_POINT('',(-0.4,0.475,-4.89858719658941E-17));
#12027=CARTESIAN_POINT('Origin',(0.,0.24,0.));
#12028=CARTESIAN_POINT('',(-0.425,0.0299999999999998,-5.20474889637625E-17));
#12029=CARTESIAN_POINT('Origin',(0.,0.0299999999999998,0.));
#12030=CARTESIAN_POINT('',(-0.425,0.24,-5.20474889637625E-17));
#12031=CARTESIAN_POINT('Origin',(0.,0.0150000000000001,0.));
#12032=CARTESIAN_POINT('',(-0.395,4.85722573273506E-17,-4.83735485663204E-17));
#12033=CARTESIAN_POINT('Origin',(0.,0.,0.));
#12034=CARTESIAN_POINT('',(-0.41,0.0150000000000001,-5.02105187650415E-17));
#12035=CARTESIAN_POINT('Origin',(0.27,0.,0.));
#12036=CARTESIAN_POINT('',(-0.27,0.,-3.30654635769785E-17));
#12037=CARTESIAN_POINT('Origin',(0.,0.,0.));
#12038=CARTESIAN_POINT('Origin',(0.,-0.02,0.));
#12039=CARTESIAN_POINT('',(-0.24505,-0.0498999999999999,3.00099698131059E-17));
#12040=CARTESIAN_POINT('Origin',(0.,-0.0498999999999999,0.));
#12041=CARTESIAN_POINT('',(-0.26,-0.02,-3.18408167778312E-17));
#12042=CARTESIAN_POINT('Origin',(0.,-0.995,0.));
#12043=CARTESIAN_POINT('',(-0.24505,-1.95495,3.00099698131059E-17));
#12044=CARTESIAN_POINT('Origin',(0.,-1.95495,0.));
#12045=CARTESIAN_POINT('',(-0.24505,-0.995,-3.00099698131059E-17));
#12046=CARTESIAN_POINT('Origin',(0.,-1.975,0.));
#12047=CARTESIAN_POINT('',(-0.2,-2.,-2.44929359829471E-17));
#12048=CARTESIAN_POINT('Origin',(0.,-2.,0.));
#12049=CARTESIAN_POINT('',(-0.225,-1.975,-2.75545529808154E-17));
#12050=CARTESIAN_POINT('Origin',(0.,-2.,0.));
#12051=CARTESIAN_POINT('Origin',(0.115470053837925,-0.5,-0.2));
#12052=CARTESIAN_POINT('',(0.23094010767585,-0.5,0.));
#12053=CARTESIAN_POINT('',(0.115470053837925,-0.5,-0.2));
#12054=CARTESIAN_POINT('',(0.23094010767585,-0.5,0.));
#12055=CARTESIAN_POINT('',(0.115470053837925,-0.8,-0.2));
#12056=CARTESIAN_POINT('',(0.115470053837925,-0.5,-0.2));
#12057=CARTESIAN_POINT('',(0.23094010767585,-0.8,0.));
#12058=CARTESIAN_POINT('',(0.23094010767585,-0.8,0.));
#12059=CARTESIAN_POINT('',(0.23094010767585,-0.5,0.));
#12060=CARTESIAN_POINT('Origin',(-0.115470053837925,-0.5,-0.2));
#12061=CARTESIAN_POINT('',(-0.115470053837925,-0.5,-0.2));
#12062=CARTESIAN_POINT('',(0.115470053837925,-0.5,-0.2));
#12063=CARTESIAN_POINT('',(-0.115470053837925,-0.8,-0.2));
#12064=CARTESIAN_POINT('',(-0.115470053837925,-0.5,-0.2));
#12065=CARTESIAN_POINT('',(0.115470053837925,-0.8,-0.2));
#12066=CARTESIAN_POINT('Origin',(-0.23094010767585,-0.5,-2.77555756156289E-17));
#12067=CARTESIAN_POINT('',(-0.23094010767585,-0.5,-2.82820063659975E-17));
#12068=CARTESIAN_POINT('',(-0.115470053837925,-0.5,-0.2));
#12069=CARTESIAN_POINT('',(-0.23094010767585,-0.8,-2.77555756156289E-17));
#12070=CARTESIAN_POINT('',(-0.23094010767585,-0.5,-2.82820063659975E-17));
#12071=CARTESIAN_POINT('',(-0.115470053837925,-0.8,-0.2));
#12072=CARTESIAN_POINT('Origin',(-0.115470053837925,-0.5,0.2));
#12073=CARTESIAN_POINT('',(-0.115470053837925,-0.5,0.2));
#12074=CARTESIAN_POINT('',(-0.23094010767585,-0.5,-2.82820063659975E-17));
#12075=CARTESIAN_POINT('',(-0.115470053837925,-0.8,0.2));
#12076=CARTESIAN_POINT('',(-0.115470053837925,-0.5,0.2));
#12077=CARTESIAN_POINT('',(-0.23094010767585,-0.8,-2.82820063659975E-17));
#12078=CARTESIAN_POINT('Origin',(0.115470053837925,-0.5,0.2));
#12079=CARTESIAN_POINT('',(0.115470053837925,-0.5,0.2));
#12080=CARTESIAN_POINT('',(-0.115470053837925,-0.5,0.2));
#12081=CARTESIAN_POINT('',(0.115470053837925,-0.8,0.2));
#12082=CARTESIAN_POINT('',(0.115470053837925,-0.5,0.2));
#12083=CARTESIAN_POINT('',(-0.115470053837925,-0.8,0.2));
#12084=CARTESIAN_POINT('Origin',(0.23094010767585,-0.5,0.));
#12085=CARTESIAN_POINT('',(0.115470053837925,-0.5,0.2));
#12086=CARTESIAN_POINT('',(0.115470053837925,-0.8,0.2));
#12087=CARTESIAN_POINT('Origin',(0.,-0.5,0.));
#12088=CARTESIAN_POINT('Origin',(0.,-0.8,0.));
#12831=UNCERTAINTY_MEASURE_WITH_UNIT(LENGTH_MEASURE(0.001),#12897,
'DISTANCE_ACCURACY_VALUE',
'Maximum model space distance between geometric entities at asserted c
onnectivities');
#12853=UNCERTAINTY_MEASURE_WITH_UNIT(LENGTH_MEASURE(0.001),#12897,
'DISTANCE_ACCURACY_VALUE',
'Maximum model space distance between geometric entities at asserted c
onnectivities');
#12874=(
GEOMETRIC_REPRESENTATION_CONTEXT(3)
GLOBAL_UNCERTAINTY_ASSIGNED_CONTEXT((#12831))
GLOBAL_UNIT_ASSIGNED_CONTEXT((#12897,#12899,#12900))
REPRESENTATION_CONTEXT('','3D')
);
#12896=(
GEOMETRIC_REPRESENTATION_CONTEXT(3)
GLOBAL_UNCERTAINTY_ASSIGNED_CONTEXT((#12853))
GLOBAL_UNIT_ASSIGNED_CONTEXT((#12897,#12899,#12900))
REPRESENTATION_CONTEXT('','3D')
);
#12897=(
LENGTH_UNIT()
NAMED_UNIT(*)
SI_UNIT(.CENTI.,.METRE.)
);
#12899=(
NAMED_UNIT(*)
PLANE_ANGLE_UNIT()
SI_UNIT($,.RADIAN.)
);
#12900=(
NAMED_UNIT(*)
SI_UNIT($,.STERADIAN.)
SOLID_ANGLE_UNIT()
);
#12921=SHAPE_DEFINITION_REPRESENTATION(#12968,#13074);
#12968=PRODUCT_DEFINITION_SHAPE('',$,#13117);
#13074=SHAPE_REPRESENTATION('',(#7042),#12874);
#13096=PRODUCT_DEFINITION_CONTEXT('part definition',#13224,'design');
#13117=PRODUCT_DEFINITION('Cap Screw - M5x20','Cap Screw - M5x20',#13159,
#13096);
#13159=PRODUCT_DEFINITION_FORMATION('',$,#13246);
#13224=APPLICATION_CONTEXT(
'Core Data for Automotive Mechanical Design Process');
#13225=PRODUCT_CONTEXT('part definition',#13224,'mechanical');
#13246=PRODUCT('Cap Screw - M5x20','Cap Screw - M5x20',
'Cap Screw - M5x20',(#13225));
#13331=COLOUR_RGB('Black',0.12,0.14,0.17);
#13332=FILL_AREA_STYLE_COLOUR('',#13331);
#13333=FILL_AREA_STYLE('',(#13332));
#13334=SURFACE_STYLE_FILL_AREA(#13333);
#13335=SURFACE_SIDE_STYLE('',(#13334));
#13336=SURFACE_STYLE_USAGE(.BOTH.,#13335);
#13337=PRESENTATION_STYLE_ASSIGNMENT((#13336));
ENDSEC;
END-ISO-10303-21;
